ISO-10303-21;
HEADER;
/* Generated by software containing ST-Developer
 * from STEP Tools, Inc. (www.steptools.com) 
 */

FILE_DESCRIPTION(
/* description */ ('Four-valve pipe header'),
/* implementation_level */ '2;1');

FILE_NAME(
/* name */ 'M4x10 Cap Screw.step',
/* time_stamp */ '2026-10-29T16:56:19-07:00',
/* author */ (''),
/* organization */ (''),
/* preprocessor_version */ 'ST-DEVELOPER v20.2',
/* originating_system */ 'Autodesk Translation Framework v15.17.0.0',
/* authorisation */ '');

FILE_SCHEMA (('AUTOMOTIVE_DESIGN { 1 0 10303 214 3 1 1 }'));
ENDSEC;

DATA;
#10=MECHANICAL_DESIGN_GEOMETRIC_PRESENTATION_REPRESENTATION('',(#358),#10119);
#237=ORIENTED_CLOSED_SHELL('',*,#5606,.F.);
#240=BREP_WITH_VOIDS('Body1',#5607,(#237));
#278=CONICAL_SURFACE('',#6502,0.325,0.785398163397448);
#279=CONICAL_SURFACE('',#6506,0.335,0.785398163397448);
#280=CONICAL_SURFACE('',#6510,0.21,0.463647609000806);
#306=SHAPE_REPRESENTATION_RELATIONSHIP('SRR','None',#10269,#332);
#332=ADVANCED_BREP_SHAPE_REPRESENTATION('',(#240),#10118);
#358=STYLED_ITEM('',(#10477),#240);
#534=FACE_BOUND('',#1517,.T.);
#736=PLANE('',#6490);
#737=PLANE('',#6491);
#738=PLANE('',#6492);
#739=PLANE('',#6493);
#740=PLANE('',#6494);
#741=PLANE('',#6495);
#742=PLANE('',#6496);
#743=PLANE('',#6497);
#744=PLANE('',#6498);
#745=PLANE('',#6500);
#746=PLANE('',#6508);
#1063=FACE_OUTER_BOUND('',#1503,.T.);
#1064=FACE_OUTER_BOUND('',#1504,.T.);
#1065=FACE_OUTER_BOUND('',#1505,.T.);
#1066=FACE_OUTER_BOUND('',#1506,.T.);
#1067=FACE_OUTER_BOUND('',#1507,.T.);
#1068=FACE_OUTER_BOUND('',#1508,.T.);
#1069=FACE_OUTER_BOUND('',#1509,.T.);
#1070=FACE_OUTER_BOUND('',#1510,.T.);
#1071=FACE_OUTER_BOUND('',#1511,.T.);
#1072=FACE_OUTER_BOUND('',#1512,.T.);
#1073=FACE_OUTER_BOUND('',#1513,.T.);
#1074=FACE_OUTER_BOUND('',#1514,.T.);
#1075=FACE_OUTER_BOUND('',#1515,.T.);
#1076=FACE_OUTER_BOUND('',#1516,.T.);
#1077=FACE_OUTER_BOUND('',#1518,.T.);
#1078=FACE_OUTER_BOUND('',#1519,.T.);
#1503=EDGE_LOOP('',(#5089,#5090,#5091,#5092));
#1504=EDGE_LOOP('',(#5093,#5094,#5095,#5096));
#1505=EDGE_LOOP('',(#5097,#5098,#5099,#5100));
#1506=EDGE_LOOP('',(#5101,#5102,#5103,#5104));
#1507=EDGE_LOOP('',(#5105,#5106,#5107,#5108));
#1508=EDGE_LOOP('',(#5109,#5110,#5111,#5112));
#1509=EDGE_LOOP('',(#5113,#5114,#5115,#5116,#5117,#5118));
#1510=EDGE_LOOP('',(#5119,#5120,#5121,#5122,#5123,#5124));
#1511=EDGE_LOOP('',(#5125));
#1512=EDGE_LOOP('',(#5126));
#1513=EDGE_LOOP('',(#5127,#5128,#5129,#5130));
#1514=EDGE_LOOP('',(#5131,#5132,#5133,#5134));
#1515=EDGE_LOOP('',(#5135,#5136,#5137,#5138));
#1516=EDGE_LOOP('',(#5139));
#1517=EDGE_LOOP('',(#5140));
#1518=EDGE_LOOP('',(#5141,#5142,#5143,#5144));
#1519=EDGE_LOOP('',(#5145,#5146,#5147,#5148));
#1915=LINE('',#9940,#2333);
#1916=LINE('',#9942,#2334);
#1917=LINE('',#9944,#2335);
#1918=LINE('',#9945,#2336);
#1919=LINE('',#9948,#2337);
#1920=LINE('',#9950,#2338);
#1921=LINE('',#9951,#2339);
#1922=LINE('',#9954,#2340);
#1923=LINE('',#9956,#2341);
#1924=LINE('',#9957,#2342);
#1925=LINE('',#9960,#2343);
#1926=LINE('',#9962,#2344);
#1927=LINE('',#9963,#2345);
#1928=LINE('',#9966,#2346);
#1929=LINE('',#9968,#2347);
#1930=LINE('',#9969,#2348);
#1931=LINE('',#9971,#2349);
#1932=LINE('',#9972,#2350);
#1933=LINE('',#9984,#2351);
#1934=LINE('',#9988,#2352);
#1935=LINE('',#9992,#2353);
#1936=LINE('',#9999,#2354);
#1937=LINE('',#10001,#2355);
#2333=VECTOR('',#8156,1.);
#2334=VECTOR('',#8157,1.);
#2335=VECTOR('',#8158,1.);
#2336=VECTOR('',#8159,1.);
#2337=VECTOR('',#8162,1.);
#2338=VECTOR('',#8163,1.);
#2339=VECTOR('',#8164,1.);
#2340=VECTOR('',#8167,1.);
#2341=VECTOR('',#8168,1.);
#2342=VECTOR('',#8169,1.);
#2343=VECTOR('',#8172,1.);
#2344=VECTOR('',#8173,1.);
#2345=VECTOR('',#8174,1.);
#2346=VECTOR('',#8177,1.);
#2347=VECTOR('',#8178,1.);
#2348=VECTOR('',#8179,1.);
#2349=VECTOR('',#8182,1.);
#2350=VECTOR('',#8183,1.);
#2351=VECTOR('',#8200,0.325);
#2352=VECTOR('',#8205,0.35);
#2353=VECTOR('',#8210,0.335);
#2354=VECTOR('',#8219,0.21);
#2355=VECTOR('',#8222,0.2);
#2573=CIRCLE('',#6499,0.1954);
#2574=CIRCLE('',#6501,0.3);
#2575=CIRCLE('',#6503,0.35);
#2576=CIRCLE('',#6505,0.35);
#2577=CIRCLE('',#6507,0.32);
#2578=CIRCLE('',#6509,0.22);
#2579=CIRCLE('',#6511,0.1954);
#3018=VERTEX_POINT('',#9938);
#3019=VERTEX_POINT('',#9939);
#3020=VERTEX_POINT('',#9941);
#3021=VERTEX_POINT('',#9943);
#3022=VERTEX_POINT('',#9947);
#3023=VERTEX_POINT('',#9949);
#3024=VERTEX_POINT('',#9953);
#3025=VERTEX_POINT('',#9955);
#3026=VERTEX_POINT('',#9959);
#3027=VERTEX_POINT('',#9961);
#3028=VERTEX_POINT('',#9965);
#3029=VERTEX_POINT('',#9967);
#3030=VERTEX_POINT('',#9976);
#3031=VERTEX_POINT('',#9979);
#3032=VERTEX_POINT('',#9982);
#3033=VERTEX_POINT('',#9986);
#3034=VERTEX_POINT('',#9990);
#3035=VERTEX_POINT('',#9994);
#3036=VERTEX_POINT('',#9997);
#3711=EDGE_CURVE('',#3018,#3019,#1915,.T.);
#3712=EDGE_CURVE('',#3019,#3020,#1916,.T.);
#3713=EDGE_CURVE('',#3020,#3021,#1917,.T.);
#3714=EDGE_CURVE('',#3018,#3021,#1918,.T.);
#3715=EDGE_CURVE('',#3019,#3022,#1919,.T.);
#3716=EDGE_CURVE('',#3022,#3023,#1920,.T.);
#3717=EDGE_CURVE('',#3023,#3020,#1921,.T.);
#3718=EDGE_CURVE('',#3022,#3024,#1922,.T.);
#3719=EDGE_CURVE('',#3024,#3025,#1923,.T.);
#3720=EDGE_CURVE('',#3025,#3023,#1924,.T.);
#3721=EDGE_CURVE('',#3024,#3026,#1925,.T.);
#3722=EDGE_CURVE('',#3026,#3027,#1926,.T.);
#3723=EDGE_CURVE('',#3027,#3025,#1927,.T.);
#3724=EDGE_CURVE('',#3026,#3028,#1928,.T.);
#3725=EDGE_CURVE('',#3028,#3029,#1929,.T.);
#3726=EDGE_CURVE('',#3029,#3027,#1930,.T.);
#3727=EDGE_CURVE('',#3028,#3018,#1931,.T.);
#3728=EDGE_CURVE('',#3021,#3029,#1932,.T.);
#3729=EDGE_CURVE('',#3030,#3030,#2573,.T.);
#3730=EDGE_CURVE('',#3031,#3031,#2574,.T.);
#3731=EDGE_CURVE('',#3032,#3032,#2575,.T.);
#3732=EDGE_CURVE('',#3032,#3031,#1933,.T.);
#3733=EDGE_CURVE('',#3033,#3033,#2576,.T.);
#3734=EDGE_CURVE('',#3033,#3032,#1934,.T.);
#3735=EDGE_CURVE('',#3034,#3034,#2577,.T.);
#3736=EDGE_CURVE('',#3034,#3033,#1935,.T.);
#3737=EDGE_CURVE('',#3035,#3035,#2578,.T.);
#3738=EDGE_CURVE('',#3036,#3036,#2579,.F.);
#3739=EDGE_CURVE('',#3036,#3035,#1936,.T.);
#3740=EDGE_CURVE('',#3030,#3036,#1937,.T.);
#5089=ORIENTED_EDGE('',*,*,#3711,.T.);
#5090=ORIENTED_EDGE('',*,*,#3712,.T.);
#5091=ORIENTED_EDGE('',*,*,#3713,.T.);
#5092=ORIENTED_EDGE('',*,*,#3714,.F.);
#5093=ORIENTED_EDGE('',*,*,#3715,.T.);
#5094=ORIENTED_EDGE('',*,*,#3716,.T.);
#5095=ORIENTED_EDGE('',*,*,#3717,.T.);
#5096=ORIENTED_EDGE('',*,*,#3712,.F.);
#5097=ORIENTED_EDGE('',*,*,#3718,.T.);
#5098=ORIENTED_EDGE('',*,*,#3719,.T.);
#5099=ORIENTED_EDGE('',*,*,#3720,.T.);
#5100=ORIENTED_EDGE('',*,*,#3716,.F.);
#5101=ORIENTED_EDGE('',*,*,#3721,.T.);
#5102=ORIENTED_EDGE('',*,*,#3722,.T.);
#5103=ORIENTED_EDGE('',*,*,#3723,.T.);
#5104=ORIENTED_EDGE('',*,*,#3719,.F.);
#5105=ORIENTED_EDGE('',*,*,#3724,.T.);
#5106=ORIENTED_EDGE('',*,*,#3725,.T.);
#5107=ORIENTED_EDGE('',*,*,#3726,.T.);
#5108=ORIENTED_EDGE('',*,*,#3722,.F.);
#5109=ORIENTED_EDGE('',*,*,#3727,.T.);
#5110=ORIENTED_EDGE('',*,*,#3714,.T.);
#5111=ORIENTED_EDGE('',*,*,#3728,.T.);
#5112=ORIENTED_EDGE('',*,*,#3725,.F.);
#5113=ORIENTED_EDGE('',*,*,#3727,.F.);
#5114=ORIENTED_EDGE('',*,*,#3724,.F.);
#5115=ORIENTED_EDGE('',*,*,#3721,.F.);
#5116=ORIENTED_EDGE('',*,*,#3718,.F.);
#5117=ORIENTED_EDGE('',*,*,#3715,.F.);
#5118=ORIENTED_EDGE('',*,*,#3711,.F.);
#5119=ORIENTED_EDGE('',*,*,#3728,.F.);
#5120=ORIENTED_EDGE('',*,*,#3713,.F.);
#5121=ORIENTED_EDGE('',*,*,#3717,.F.);
#5122=ORIENTED_EDGE('',*,*,#3720,.F.);
#5123=ORIENTED_EDGE('',*,*,#3723,.F.);
#5124=ORIENTED_EDGE('',*,*,#3726,.F.);
#5125=ORIENTED_EDGE('',*,*,#3729,.F.);
#5126=ORIENTED_EDGE('',*,*,#3730,.F.);
#5127=ORIENTED_EDGE('',*,*,#3731,.F.);
#5128=ORIENTED_EDGE('',*,*,#3732,.T.);
#5129=ORIENTED_EDGE('',*,*,#3730,.T.);
#5130=ORIENTED_EDGE('',*,*,#3732,.F.);
#5131=ORIENTED_EDGE('',*,*,#3733,.F.);
#5132=ORIENTED_EDGE('',*,*,#3734,.T.);
#5133=ORIENTED_EDGE('',*,*,#3731,.T.);
#5134=ORIENTED_EDGE('',*,*,#3734,.F.);
#5135=ORIENTED_EDGE('',*,*,#3735,.F.);
#5136=ORIENTED_EDGE('',*,*,#3736,.T.);
#5137=ORIENTED_EDGE('',*,*,#3733,.T.);
#5138=ORIENTED_EDGE('',*,*,#3736,.F.);
#5139=ORIENTED_EDGE('',*,*,#3735,.T.);
#5140=ORIENTED_EDGE('',*,*,#3737,.F.);
#5141=ORIENTED_EDGE('',*,*,#3738,.F.);
#5142=ORIENTED_EDGE('',*,*,#3739,.T.);
#5143=ORIENTED_EDGE('',*,*,#3737,.T.);
#5144=ORIENTED_EDGE('',*,*,#3739,.F.);
#5145=ORIENTED_EDGE('',*,*,#3729,.T.);
#5146=ORIENTED_EDGE('',*,*,#3740,.T.);
#5147=ORIENTED_EDGE('',*,*,#3738,.T.);
#5148=ORIENTED_EDGE('',*,*,#3740,.F.);
#5245=CYLINDRICAL_SURFACE('',#6504,0.35);
#5246=CYLINDRICAL_SURFACE('',#6512,0.1954);
#5563=ADVANCED_FACE('',(#1063),#736,.F.);
#5564=ADVANCED_FACE('',(#1064),#737,.F.);
#5565=ADVANCED_FACE('',(#1065),#738,.F.);
#5566=ADVANCED_FACE('',(#1066),#739,.F.);
#5567=ADVANCED_FACE('',(#1067),#740,.F.);
#5568=ADVANCED_FACE('',(#1068),#741,.F.);
#5569=ADVANCED_FACE('',(#1069),#742,.F.);
#5570=ADVANCED_FACE('',(#1070),#743,.F.);
#5571=ADVANCED_FACE('',(#1071),#744,.F.);
#5572=ADVANCED_FACE('',(#1072),#745,.T.);
#5573=ADVANCED_FACE('',(#1073),#278,.T.);
#5574=ADVANCED_FACE('',(#1074),#5245,.T.);
#5575=ADVANCED_FACE('',(#1075),#279,.T.);
#5576=ADVANCED_FACE('',(#1076,#534),#746,.T.);
#5577=ADVANCED_FACE('',(#1077),#280,.T.);
#5578=ADVANCED_FACE('',(#1078),#5246,.T.);
#5606=CLOSED_SHELL('',(#5563,#5564,#5565,#5566,#5567,#5568,#5569,#5570));
#5607=CLOSED_SHELL('',(#5571,#5572,#5573,#5574,#5575,#5576,#5577,#5578));
#6489=AXIS2_PLACEMENT_3D('',#9936,#8152,#8153);
#6490=AXIS2_PLACEMENT_3D('',#9937,#8154,#8155);
#6491=AXIS2_PLACEMENT_3D('',#9946,#8160,#8161);
#6492=AXIS2_PLACEMENT_3D('',#9952,#8165,#8166);
#6493=AXIS2_PLACEMENT_3D('',#9958,#8170,#8171);
#6494=AXIS2_PLACEMENT_3D('',#9964,#8175,#8176);
#6495=AXIS2_PLACEMENT_3D('',#9970,#8180,#8181);
#6496=AXIS2_PLACEMENT_3D('',#9973,#8184,#8185);
#6497=AXIS2_PLACEMENT_3D('',#9974,#8186,#8187);
#6498=AXIS2_PLACEMENT_3D('',#9975,#8188,#8189);
#6499=AXIS2_PLACEMENT_3D('',#9977,#8190,#8191);
#6500=AXIS2_PLACEMENT_3D('',#9978,#8192,#8193);
#6501=AXIS2_PLACEMENT_3D('',#9980,#8194,#8195);
#6502=AXIS2_PLACEMENT_3D('',#9981,#8196,#8197);
#6503=AXIS2_PLACEMENT_3D('',#9983,#8198,#8199);
#6504=AXIS2_PLACEMENT_3D('',#9985,#8201,#8202);
#6505=AXIS2_PLACEMENT_3D('',#9987,#8203,#8204);
#6506=AXIS2_PLACEMENT_3D('',#9989,#8206,#8207);
#6507=AXIS2_PLACEMENT_3D('',#9991,#8208,#8209);
#6508=AXIS2_PLACEMENT_3D('',#9993,#8211,#8212);
#6509=AXIS2_PLACEMENT_3D('',#9995,#8213,#8214);
#6510=AXIS2_PLACEMENT_3D('',#9996,#8215,#8216);
#6511=AXIS2_PLACEMENT_3D('',#9998,#8217,#8218);
#6512=AXIS2_PLACEMENT_3D('',#10000,#8220,#8221);
#8152=DIRECTION('axis',(0.,0.,1.));
#8153=DIRECTION('refdir',(1.,0.,0.));
#8154=DIRECTION('center_axis',(0.866025403784439,0.,-0.5));
#8155=DIRECTION('ref_axis',(0.5,0.,0.866025403784439));
#8156=DIRECTION('',(-0.5,0.,-0.866025403784439));
#8157=DIRECTION('',(0.,-1.,0.));
#8158=DIRECTION('',(0.5,0.,0.866025403784439));
#8159=DIRECTION('',(0.,-1.,0.));
#8160=DIRECTION('center_axis',(1.60246890531964E-16,0.,-1.));
#8161=DIRECTION('ref_axis',(1.,0.,1.60246890531964E-16));
#8162=DIRECTION('',(-1.,0.,-1.60246890531964E-16));
#8163=DIRECTION('',(0.,-1.,0.));
#8164=DIRECTION('',(1.,0.,1.60246890531964E-16));
#8165=DIRECTION('center_axis',(-0.866025403784439,0.,-0.5));
#8166=DIRECTION('ref_axis',(0.5,0.,-0.866025403784439));
#8167=DIRECTION('',(-0.5,0.,0.866025403784439));
#8168=DIRECTION('',(0.,-1.,0.));
#8169=DIRECTION('',(0.5,0.,-0.866025403784439));
#8170=DIRECTION('center_axis',(-0.866025403784439,0.,0.5));
#8171=DIRECTION('ref_axis',(-0.5,0.,-0.866025403784439));
#8172=DIRECTION('',(0.5,0.,0.866025403784439));
#8173=DIRECTION('',(0.,-1.,0.));
#8174=DIRECTION('',(-0.5,0.,-0.866025403784439));
#8175=DIRECTION('center_axis',(-1.60246890531964E-16,0.,1.));
#8176=DIRECTION('ref_axis',(-1.,0.,-1.60246890531964E-16));
#8177=DIRECTION('',(1.,0.,1.60246890531964E-16));
#8178=DIRECTION('',(0.,-1.,0.));
#8179=DIRECTION('',(-1.,0.,-1.60246890531964E-16));
#8180=DIRECTION('center_axis',(0.866025403784439,0.,0.5));
#8181=DIRECTION('ref_axis',(-0.5,0.,0.866025403784439));
#8182=DIRECTION('',(0.5,0.,-0.866025403784439));
#8183=DIRECTION('',(-0.5,0.,0.866025403784439));
#8184=DIRECTION('center_axis',(0.,1.,0.));
#8185=DIRECTION('ref_axis',(1.,0.,0.));
#8186=DIRECTION('center_axis',(0.,-1.,0.));
#8187=DIRECTION('ref_axis',(0.,0.,-1.));
#8188=DIRECTION('center_axis',(0.,1.,0.));
#8189=DIRECTION('ref_axis',(1.,0.,0.));
#8190=DIRECTION('center_axis',(0.,1.,0.));
#8191=DIRECTION('ref_axis',(1.,0.,0.));
#8192=DIRECTION('center_axis',(0.,1.,0.));
#8193=DIRECTION('ref_axis',(0.,0.,1.));
#8194=DIRECTION('center_axis',(0.,-1.,0.));
#8195=DIRECTION('ref_axis',(1.,0.,0.));
#8196=DIRECTION('center_axis',(0.,-1.,0.));
#8197=DIRECTION('ref_axis',(1.,0.,0.));
#8198=DIRECTION('center_axis',(0.,-1.,0.));
#8199=DIRECTION('ref_axis',(1.,0.,0.));
#8200=DIRECTION('',(0.707106781186547,0.707106781186548,8.65956056235493E-17));
#8201=DIRECTION('center_axis',(0.,-1.,0.));
#8202=DIRECTION('ref_axis',(1.,0.,0.));
#8203=DIRECTION('center_axis',(0.,-1.,0.));
#8204=DIRECTION('ref_axis',(1.,0.,0.));
#8205=DIRECTION('',(0.,1.,0.));
#8206=DIRECTION('center_axis',(0.,1.,0.));
#8207=DIRECTION('ref_axis',(1.,0.,0.));
#8208=DIRECTION('center_axis',(0.,-1.,0.));
#8209=DIRECTION('ref_axis',(1.,0.,0.));
#8210=DIRECTION('',(-0.707106781186547,0.707106781186548,-8.65956056235493E-17));
#8211=DIRECTION('center_axis',(0.,-1.,0.));
#8212=DIRECTION('ref_axis',(0.,0.,-1.));
#8213=DIRECTION('center_axis',(0.,-1.,0.));
#8214=DIRECTION('ref_axis',(1.,0.,0.));
#8215=DIRECTION('center_axis',(0.,1.,0.));
#8216=DIRECTION('ref_axis',(1.,0.,0.));
#8217=DIRECTION('center_axis',(0.,1.,0.));
#8218=DIRECTION('ref_axis',(1.,0.,0.));
#8219=DIRECTION('',(-0.447213595499958,0.894427190999916,-5.47678698264203E-17));
#8220=DIRECTION('center_axis',(0.,-1.,0.));
#8221=DIRECTION('ref_axis',(1.,0.,0.));
#8222=DIRECTION('',(0.,1.,0.));
#9936=CARTESIAN_POINT('',(0.,0.,0.));
#9937=CARTESIAN_POINT('Origin',(0.0866025403784439,-0.4,-0.15));
#9938=CARTESIAN_POINT('',(0.173205080756888,-0.4,0.));
#9939=CARTESIAN_POINT('',(0.0866025403784439,-0.4,-0.15));
#9940=CARTESIAN_POINT('',(0.173205080756888,-0.4,0.));
#9941=CARTESIAN_POINT('',(0.0866025403784439,-0.64,-0.15));
#9942=CARTESIAN_POINT('',(0.0866025403784439,-0.4,-0.15));
#9943=CARTESIAN_POINT('',(0.173205080756888,-0.64,0.));
#9944=CARTESIAN_POINT('',(0.173205080756888,-0.64,0.));
#9945=CARTESIAN_POINT('',(0.173205080756888,-0.4,0.));
#9946=CARTESIAN_POINT('Origin',(-0.0866025403784438,-0.4,-0.15));
#9947=CARTESIAN_POINT('',(-0.0866025403784438,-0.4,-0.15));
#9948=CARTESIAN_POINT('',(0.0866025403784439,-0.4,-0.15));
#9949=CARTESIAN_POINT('',(-0.0866025403784438,-0.64,-0.15));
#9950=CARTESIAN_POINT('',(-0.0866025403784438,-0.4,-0.15));
#9951=CARTESIAN_POINT('',(0.0866025403784439,-0.64,-0.15));
#9952=CARTESIAN_POINT('Origin',(-0.173205080756888,-0.4,-2.77555756156289E-17));
#9953=CARTESIAN_POINT('',(-0.173205080756888,-0.4,-2.12115047744981E-17));
#9954=CARTESIAN_POINT('',(-0.0866025403784438,-0.4,-0.15));
#9955=CARTESIAN_POINT('',(-0.173205080756888,-0.64,-2.77555756156289E-17));
#9956=CARTESIAN_POINT('',(-0.173205080756888,-0.4,-2.12115047744981E-17));
#9957=CARTESIAN_POINT('',(-0.0866025403784438,-0.64,-0.15));
#9958=CARTESIAN_POINT('Origin',(-0.0866025403784439,-0.4,0.15));
#9959=CARTESIAN_POINT('',(-0.0866025403784439,-0.4,0.15));
#9960=CARTESIAN_POINT('',(-0.173205080756888,-0.4,-2.12115047744981E-17));
#9961=CARTESIAN_POINT('',(-0.0866025403784439,-0.64,0.15));
#9962=CARTESIAN_POINT('',(-0.0866025403784439,-0.4,0.15));
#9963=CARTESIAN_POINT('',(-0.173205080756888,-0.64,-2.12115047744981E-17));
#9964=CARTESIAN_POINT('Origin',(0.0866025403784439,-0.4,0.15));
#9965=CARTESIAN_POINT('',(0.0866025403784439,-0.4,0.15));
#9966=CARTESIAN_POINT('',(-0.0866025403784439,-0.4,0.15));
#9967=CARTESIAN_POINT('',(0.0866025403784439,-0.64,0.15));
#9968=CARTESIAN_POINT('',(0.0866025403784439,-0.4,0.15));
#9969=CARTESIAN_POINT('',(-0.0866025403784439,-0.64,0.15));
#9970=CARTESIAN_POINT('Origin',(0.173205080756888,-0.4,0.));
#9971=CARTESIAN_POINT('',(0.0866025403784439,-0.4,0.15));
#9972=CARTESIAN_POINT('',(0.0866025403784439,-0.64,0.15));
#9973=CARTESIAN_POINT('Origin',(0.,-0.4,-2.77555756156289E-17));
#9974=CARTESIAN_POINT('Origin',(0.,-0.64,-2.77555756156289E-17));
#9975=CARTESIAN_POINT('Origin',(0.,-1.,0.));
#9976=CARTESIAN_POINT('',(-0.1954,-1.,2.39295984553393E-17));
#9977=CARTESIAN_POINT('Origin',(0.,-1.,0.));
#9978=CARTESIAN_POINT('Origin',(0.3,0.4,0.));
#9979=CARTESIAN_POINT('',(-0.3,0.4,-3.67394039744206E-17));
#9980=CARTESIAN_POINT('Origin',(0.,0.4,0.));
#9981=CARTESIAN_POINT('Origin',(0.,0.375,0.));
#9982=CARTESIAN_POINT('',(-0.35,0.35,-4.28626379701573E-17));
#9983=CARTESIAN_POINT('Origin',(0.,0.35,0.));
#9984=CARTESIAN_POINT('',(-0.325,0.375,-3.9801020972289E-17));
#9985=CARTESIAN_POINT('Origin',(0.,0.19,0.));
#9986=CARTESIAN_POINT('',(-0.35,0.03,-4.28626379701574E-17));
#9987=CARTESIAN_POINT('Origin',(0.,0.03,0.));
#9988=CARTESIAN_POINT('',(-0.35,0.19,-4.28626379701574E-17));
#9989=CARTESIAN_POINT('Origin',(0.,0.0149999999999999,0.));
#9990=CARTESIAN_POINT('',(-0.32,-3.29597460435593E-17,-3.91886975727153E-17));
#9991=CARTESIAN_POINT('Origin',(0.,0.,0.));
#9992=CARTESIAN_POINT('',(-0.335,0.0149999999999999,-4.10256677714363E-17));
#9993=CARTESIAN_POINT('Origin',(0.22,0.,0.));
#9994=CARTESIAN_POINT('',(-0.22,-6.93889390390723E-18,-2.69422295812418E-17));
#9995=CARTESIAN_POINT('Origin',(0.,0.,0.));
#9996=CARTESIAN_POINT('Origin',(0.,-0.02,0.));
#9997=CARTESIAN_POINT('',(-0.1954,-0.0492,2.39295984553393E-17));
#9998=CARTESIAN_POINT('Origin',(0.,-0.0492,0.));
#9999=CARTESIAN_POINT('',(-0.21,-0.02,-2.57175827820944E-17));
#10000=CARTESIAN_POINT('Origin',(0.,-0.8,0.));
#10001=CARTESIAN_POINT('',(-0.1954,-0.8,-2.39295984553393E-17));
#10087=UNCERTAINTY_MEASURE_WITH_UNIT(LENGTH_MEASURE(0.001),#10120,
'DISTANCE_ACCURACY_VALUE',
'Maximum model space distance between geometric entities at asserted c
onnectivities');
#10088=UNCERTAINTY_MEASURE_WITH_UNIT(LENGTH_MEASURE(0.001),#10120,
'DISTANCE_ACCURACY_VALUE',
'Maximum model space distance between geometric entities at asserted c
onnectivities');
#10118=(
GEOMETRIC_REPRESENTATION_CONTEXT(3)
GLOBAL_UNCERTAINTY_ASSIGNED_CONTEXT((#10087))
GLOBAL_UNIT_ASSIGNED_CONTEXT((#10120,#10122,#10123))
REPRESENTATION_CONTEXT('','3D')
);
#10119=(
GEOMETRIC_REPRESENTATION_CONTEXT(3)
GLOBAL_UNCERTAINTY_ASSIGNED_CONTEXT((#10088))
GLOBAL_UNIT_ASSIGNED_CONTEXT((#10120,#10122,#10123))
REPRESENTATION_CONTEXT('','3D')
);
#10120=(
LENGTH_UNIT()
NAMED_UNIT(*)
SI_UNIT(.CENTI.,.METRE.)
);
#10122=(
NAMED_UNIT(*)
PLANE_ANGLE_UNIT()
SI_UNIT($,.RADIAN.)
);
#10123=(
NAMED_UNIT(*)
SI_UNIT($,.STERADIAN.)
SOLID_ANGLE_UNIT()
);
#10153=SHAPE_DEFINITION_REPRESENTATION(#10183,#10269);
#10183=PRODUCT_DEFINITION_SHAPE('',$,#10300);
#10269=SHAPE_REPRESENTATION('',(#6489),#10118);
#10270=PRODUCT_DEFINITION_CONTEXT('part definition',#10362,'design');
#10300=PRODUCT_DEFINITION('M4x10 Cap Screw','M4x10 Cap Screw',#10330,#10270);
#10330=PRODUCT_DEFINITION_FORMATION('',$,#10393);
#10362=APPLICATION_CONTEXT(
'Core Data for Automotive Mechanical Design Process');
#10363=PRODUCT_CONTEXT('part definition',#10362,'mechanical');
#10393=PRODUCT('M4x10 Cap Screw','M4x10 Cap Screw','M4x10 Cap Screw',(#10363));
#10471=COLOUR_RGB('Black',0.12,0.14,0.17);
#10472=FILL_AREA_STYLE_COLOUR('',#10471);
#10473=FILL_AREA_STYLE('',(#10472));
#10474=SURFACE_STYLE_FILL_AREA(#10473);
#10475=SURFACE_SIDE_STYLE('',(#10474));
#10476=SURFACE_STYLE_USAGE(.BOTH.,#10475);
#10477=PRESENTATION_STYLE_ASSIGNMENT((#10476));
ENDSEC;
END-ISO-10303-21;
